ISO-10303-21;
HEADER;
/* Generated by software containing ST-Developer
 * from STEP Tools, Inc. (www.steptools.com) 
 */

FILE_DESCRIPTION(
/* description */ ('Shaft runout checking stand'),
/* implementation_level */ '2;1');

FILE_NAME(
/* name */ 'Inner race spacer (7).step',
/* time_stamp */ '2026-11-02T21:12:33-08:00',
/* author */ (''),
/* organization */ (''),
/* preprocessor_version */ 'ST-DEVELOPER v20.2',
/* originating_system */ 'Autodesk Translation Framework v15.17.0.0',
/* authorisation */ '');

FILE_SCHEMA (('AUTOMOTIVE_DESIGN { 1 0 10303 214 3 1 1 }'));
ENDSEC;

DATA;
#10=MECHANICAL_DESIGN_GEOMETRIC_PRESENTATION_REPRESENTATION('',(#483),#11748);
#397=SHAPE_REPRESENTATION_RELATIONSHIP('SRR','None',#11946,#440);
#440=ADVANCED_BREP_SHAPE_REPRESENTATION('',(#533),#11722);
#483=STYLED_ITEM('',(#12170),#533);
#533=MANIFOLD_SOLID_BREP('Body1',#6227);
#630=FACE_BOUND('',#1673,.T.);
#631=FACE_BOUND('',#1675,.T.);
#787=CIRCLE('',#7070,0.505);
#788=CIRCLE('',#7071,0.505);
#789=CIRCLE('',#7073,0.7);
#790=CIRCLE('',#7074,0.7);
#992=CYLINDRICAL_SURFACE('',#7069,0.505);
#993=CYLINDRICAL_SURFACE('',#7072,0.7);
#1234=FACE_OUTER_BOUND('',#1670,.T.);
#1235=FACE_OUTER_BOUND('',#1671,.T.);
#1236=FACE_OUTER_BOUND('',#1672,.T.);
#1237=FACE_OUTER_BOUND('',#1674,.T.);
#1670=EDGE_LOOP('',(#4956,#4957,#4958,#4959));
#1671=EDGE_LOOP('',(#4960,#4961,#4962,#4963));
#1672=EDGE_LOOP('',(#4964));
#1673=EDGE_LOOP('',(#4965));
#1674=EDGE_LOOP('',(#4966));
#1675=EDGE_LOOP('',(#4967));
#2203=LINE('',#10420,#2670);
#2204=LINE('',#10426,#2671);
#2670=VECTOR('',#8484,0.505);
#2671=VECTOR('',#8491,0.7);
#3107=VERTEX_POINT('',#10417);
#3108=VERTEX_POINT('',#10419);
#3109=VERTEX_POINT('',#10423);
#3110=VERTEX_POINT('',#10425);
#3764=EDGE_CURVE('',#3107,#3107,#787,.T.);
#3765=EDGE_CURVE('',#3107,#3108,#2203,.T.);
#3766=EDGE_CURVE('',#3108,#3108,#788,.T.);
#3767=EDGE_CURVE('',#3109,#3109,#789,.T.);
#3768=EDGE_CURVE('',#3109,#3110,#2204,.T.);
#3769=EDGE_CURVE('',#3110,#3110,#790,.T.);
#4956=ORIENTED_EDGE('',*,*,#3764,.F.);
#4957=ORIENTED_EDGE('',*,*,#3765,.T.);
#4958=ORIENTED_EDGE('',*,*,#3766,.T.);
#4959=ORIENTED_EDGE('',*,*,#3765,.F.);
#4960=ORIENTED_EDGE('',*,*,#3767,.F.);
#4961=ORIENTED_EDGE('',*,*,#3768,.T.);
#4962=ORIENTED_EDGE('',*,*,#3769,.T.);
#4963=ORIENTED_EDGE('',*,*,#3768,.F.);
#4964=ORIENTED_EDGE('',*,*,#3767,.T.);
#4965=ORIENTED_EDGE('',*,*,#3764,.T.);
#4966=ORIENTED_EDGE('',*,*,#3769,.F.);
#4967=ORIENTED_EDGE('',*,*,#3766,.F.);
#5742=PLANE('',#7075);
#5743=PLANE('',#7076);
#6034=ADVANCED_FACE('',(#1234),#992,.F.);
#6035=ADVANCED_FACE('',(#1235),#993,.T.);
#6036=ADVANCED_FACE('',(#1236,#630),#5742,.T.);
#6037=ADVANCED_FACE('',(#1237,#631),#5743,.F.);
#6227=CLOSED_SHELL('',(#6034,#6035,#6036,#6037));
#7068=AXIS2_PLACEMENT_3D('',#10415,#8478,#8479);
#7069=AXIS2_PLACEMENT_3D('',#10416,#8480,#8481);
#7070=AXIS2_PLACEMENT_3D('',#10418,#8482,#8483);
#7071=AXIS2_PLACEMENT_3D('',#10421,#8485,#8486);
#7072=AXIS2_PLACEMENT_3D('',#10422,#8487,#8488);
#7073=AXIS2_PLACEMENT_3D('',#10424,#8489,#8490);
#7074=AXIS2_PLACEMENT_3D('',#10427,#8492,#8493);
#7075=AXIS2_PLACEMENT_3D('',#10428,#8494,#8495);
#7076=AXIS2_PLACEMENT_3D('',#10429,#8496,#8497);
#8478=DIRECTION('axis',(0.,0.,1.));
#8479=DIRECTION('refdir',(1.,0.,0.));
#8480=DIRECTION('center_axis',(0.,1.,0.));
#8481=DIRECTION('ref_axis',(1.,0.,0.));
#8482=DIRECTION('center_axis',(0.,-1.,0.));
#8483=DIRECTION('ref_axis',(1.,0.,0.));
#8484=DIRECTION('',(0.,-1.,0.));
#8485=DIRECTION('center_axis',(0.,-1.,0.));
#8486=DIRECTION('ref_axis',(1.,0.,0.));
#8487=DIRECTION('center_axis',(0.,1.,0.));
#8488=DIRECTION('ref_axis',(1.,0.,0.));
#8489=DIRECTION('center_axis',(0.,1.,0.));
#8490=DIRECTION('ref_axis',(1.,0.,0.));
#8491=DIRECTION('',(0.,-1.,0.));
#8492=DIRECTION('center_axis',(0.,1.,0.));
#8493=DIRECTION('ref_axis',(1.,0.,0.));
#8494=DIRECTION('center_axis',(0.,1.,0.));
#8495=DIRECTION('ref_axis',(1.,0.,0.));
#8496=DIRECTION('center_axis',(0.,1.,0.));
#8497=DIRECTION('ref_axis',(1.,0.,0.));
#10415=CARTESIAN_POINT('',(0.,0.,0.));
#10416=CARTESIAN_POINT('Origin',(2.,10.45,5.));
#10417=CARTESIAN_POINT('',(1.495,10.8,5.));
#10418=CARTESIAN_POINT('Origin',(2.,10.8,5.));
#10419=CARTESIAN_POINT('',(1.495,10.45,5.));
#10420=CARTESIAN_POINT('',(1.495,10.45,5.));
#10421=CARTESIAN_POINT('Origin',(2.,10.45,5.));
#10422=CARTESIAN_POINT('Origin',(2.,10.45,5.));
#10423=CARTESIAN_POINT('',(1.3,10.8,5.));
#10424=CARTESIAN_POINT('Origin',(2.,10.8,5.));
#10425=CARTESIAN_POINT('',(1.3,10.45,5.));
#10426=CARTESIAN_POINT('',(1.3,10.45,5.));
#10427=CARTESIAN_POINT('Origin',(2.,10.45,5.));
#10428=CARTESIAN_POINT('Origin',(2.,10.8,5.));
#10429=CARTESIAN_POINT('Origin',(2.,10.45,5.));
#11673=UNCERTAINTY_MEASURE_WITH_UNIT(LENGTH_MEASURE(0.001),#11749,
'DISTANCE_ACCURACY_VALUE',
'Maximum model space distance between geometric entities at asserted c
onnectivities');
#11699=UNCERTAINTY_MEASURE_WITH_UNIT(LENGTH_MEASURE(0.001),#11749,
'DISTANCE_ACCURACY_VALUE',
'Maximum model space distance between geometric entities at asserted c
onnectivities');
#11722=(
GEOMETRIC_REPRESENTATION_CONTEXT(3)
GLOBAL_UNCERTAINTY_ASSIGNED_CONTEXT((#11673))
GLOBAL_UNIT_ASSIGNED_CONTEXT((#11749,#11751,#11752))
REPRESENTATION_CONTEXT('','3D')
);
#11748=(
GEOMETRIC_REPRESENTATION_CONTEXT(3)
GLOBAL_UNCERTAINTY_ASSIGNED_CONTEXT((#11699))
GLOBAL_UNIT_ASSIGNED_CONTEXT((#11749,#11751,#11752))
REPRESENTATION_CONTEXT('','3D')
);
#11749=(
LENGTH_UNIT()
NAMED_UNIT(*)
SI_UNIT(.CENTI.,.METRE.)
);
#11751=(
NAMED_UNIT(*)
PLANE_ANGLE_UNIT()
SI_UNIT($,.RADIAN.)
);
#11752=(
NAMED_UNIT(*)
SI_UNIT($,.STERADIAN.)
SOLID_ANGLE_UNIT()
);
#11775=SHAPE_DEFINITION_REPRESENTATION(#11823,#11946);
#11823=PRODUCT_DEFINITION_SHAPE('',$,#11995);
#11946=SHAPE_REPRESENTATION('',(#7068),#11722);
#11972=PRODUCT_DEFINITION_CONTEXT('part definition',#12118,'design');
#11995=PRODUCT_DEFINITION('Inner race spacer_4','Inner race spacer (7)',
#12043,#11972);
#12043=PRODUCT_DEFINITION_FORMATION('',$,#12142);
#12118=APPLICATION_CONTEXT(
'Core Data for Automotive Mechanical Design Process');
#12119=PRODUCT_CONTEXT('part definition',#12118,'mechanical');
#12142=PRODUCT('Inner race spacer_4','Inner race spacer (7)',
'Inner race spacer',(#12119));
#12170=PRESENTATION_STYLE_ASSIGNMENT((#12175));
#12175=SURFACE_STYLE_USAGE(.BOTH.,#12180);
#12180=SURFACE_SIDE_STYLE('',(#12185));
#12185=SURFACE_STYLE_FILL_AREA(#12190);
#12190=FILL_AREA_STYLE('CAD Library Painted - Steel gray',(#12195));
#12195=FILL_AREA_STYLE_COLOUR('CAD Library Painted - Steel gray',#12200);
#12200=COLOUR_RGB('CAD Library Painted - Steel gray',0.592156862745098,
0.631372549019608,0.67843137254902);
ENDSEC;
END-ISO-10303-21;
